ISO-10303-21;
HEADER;
/* Generated by software containing ST-Developer
 * from STEP Tools, Inc. (www.steptools.com) 
 */

FILE_DESCRIPTION(
/* description */ (''),
/* implementation_level */ '2;1');

FILE_NAME(
/* name */ 'Blade_01.step',
/* time_stamp */ '2026-10-23T22:28:14+06:00',
/* author */ (''),
/* organization */ (''),
/* preprocessor_version */ 'ST-DEVELOPER v20.2',
/* originating_system */ 'Autodesk Translation Framework v15.15.0.0',
/* authorisation */ '');

FILE_SCHEMA (('AUTOMOTIVE_DESIGN { 1 0 10303 214 3 1 1 }'));
ENDSEC;

DATA;
#10=MECHANICAL_DESIGN_GEOMETRIC_PRESENTATION_REPRESENTATION('',(#105),#6753);
#79=SHAPE_REPRESENTATION_RELATIONSHIP('SRR','None',#6802,#92);
#92=ADVANCED_BREP_SHAPE_REPRESENTATION('',(#118),#6742);
#105=STYLED_ITEM('',(#6935),#118);
#118=MANIFOLD_SOLID_BREP('Blade_01',#3754);
#132=FACE_BOUND('',#566,.T.);
#133=FACE_BOUND('',#567,.T.);
#194=PLANE('',#3942);
#195=PLANE('',#3943);
#196=PLANE('',#3944);
#197=PLANE('',#3951);
#198=PLANE('',#3954);
#199=PLANE('',#3959);
#347=FACE_OUTER_BOUND('',#563,.T.);
#348=FACE_OUTER_BOUND('',#564,.T.);
#349=FACE_OUTER_BOUND('',#565,.T.);
#350=FACE_OUTER_BOUND('',#568,.T.);
#351=FACE_OUTER_BOUND('',#569,.T.);
#352=FACE_OUTER_BOUND('',#570,.T.);
#353=FACE_OUTER_BOUND('',#571,.T.);
#354=FACE_OUTER_BOUND('',#572,.T.);
#355=FACE_OUTER_BOUND('',#573,.T.);
#356=FACE_OUTER_BOUND('',#574,.T.);
#563=EDGE_LOOP('',(#2512,#2513,#2514,#2515));
#564=EDGE_LOOP('',(#2516,#2517,#2518,#2519));
#565=EDGE_LOOP('',(#2520,#2521,#2522,#2523));
#566=EDGE_LOOP('',(#2524));
#567=EDGE_LOOP('',(#2525));
#568=EDGE_LOOP('',(#2526,#2527,#2528,#2529));
#569=EDGE_LOOP('',(#2530));
#570=EDGE_LOOP('',(#2531,#2532,#2533,#2534));
#571=EDGE_LOOP('',(#2535));
#572=EDGE_LOOP('',(#2536,#2537,#2538,#2539));
#573=EDGE_LOOP('',(#2540,#2541,#2542,#2543));
#574=EDGE_LOOP('',(#2544,#2545,#2546,#2547));
#831=CIRCLE('',#3945,33.8);
#832=CIRCLE('',#3946,4.99999999999999);
#833=CIRCLE('',#3947,1.1);
#834=CIRCLE('',#3948,1.1);
#835=CIRCLE('',#3950,1.1);
#836=CIRCLE('',#3953,1.1);
#837=CIRCLE('',#3956,4.99999999999999);
#838=CIRCLE('',#3958,33.8);
#1045=LINE('',#5631,#1331);
#1046=LINE('',#5633,#1332);
#1047=LINE('',#5635,#1333);
#1048=LINE('',#5636,#1334);
#1049=LINE('',#5640,#1335);
#1050=LINE('',#5642,#1336);
#1051=LINE('',#5644,#1337);
#1052=LINE('',#5645,#1338);
#1053=LINE('',#5656,#1339);
#1054=LINE('',#5661,#1340);
#1331=VECTOR('',#4446,10.);
#1332=VECTOR('',#4447,10.);
#1333=VECTOR('',#4448,10.);
#1334=VECTOR('',#4449,10.);
#1335=VECTOR('',#4452,10.);
#1336=VECTOR('',#4453,10.);
#1337=VECTOR('',#4454,10.);
#1338=VECTOR('',#4455,10.);
#1339=VECTOR('',#4470,1.1);
#1340=VECTOR('',#4477,1.1);
#1623=VERTEX_POINT('',#5629);
#1624=VERTEX_POINT('',#5630);
#1625=VERTEX_POINT('',#5632);
#1626=VERTEX_POINT('',#5634);
#1627=VERTEX_POINT('',#5638);
#1628=VERTEX_POINT('',#5639);
#1629=VERTEX_POINT('',#5641);
#1630=VERTEX_POINT('',#5643);
#1631=VERTEX_POINT('',#5649);
#1632=VERTEX_POINT('',#5651);
#1633=VERTEX_POINT('',#5654);
#1634=VERTEX_POINT('',#5659);
#1973=EDGE_CURVE('',#1623,#1624,#1045,.T.);
#1974=EDGE_CURVE('',#1625,#1623,#1046,.T.);
#1975=EDGE_CURVE('',#1626,#1625,#1047,.T.);
#1976=EDGE_CURVE('',#1624,#1626,#1048,.T.);
#1977=EDGE_CURVE('',#1627,#1628,#1049,.T.);
#1978=EDGE_CURVE('',#1629,#1627,#1050,.T.);
#1979=EDGE_CURVE('',#1630,#1629,#1051,.T.);
#1980=EDGE_CURVE('',#1628,#1630,#1052,.T.);
#1981=EDGE_CURVE('',#1627,#1624,#831,.T.);
#1982=EDGE_CURVE('',#1623,#1628,#832,.T.);
#1983=EDGE_CURVE('',#1631,#1631,#833,.T.);
#1984=EDGE_CURVE('',#1632,#1632,#834,.T.);
#1985=EDGE_CURVE('',#1633,#1633,#835,.T.);
#1986=EDGE_CURVE('',#1633,#1631,#1053,.T.);
#1987=EDGE_CURVE('',#1634,#1634,#836,.T.);
#1988=EDGE_CURVE('',#1634,#1632,#1054,.T.);
#1989=EDGE_CURVE('',#1625,#1630,#837,.T.);
#1990=EDGE_CURVE('',#1629,#1626,#838,.T.);
#2512=ORIENTED_EDGE('',*,*,#1973,.F.);
#2513=ORIENTED_EDGE('',*,*,#1974,.F.);
#2514=ORIENTED_EDGE('',*,*,#1975,.F.);
#2515=ORIENTED_EDGE('',*,*,#1976,.F.);
#2516=ORIENTED_EDGE('',*,*,#1977,.F.);
#2517=ORIENTED_EDGE('',*,*,#1978,.F.);
#2518=ORIENTED_EDGE('',*,*,#1979,.F.);
#2519=ORIENTED_EDGE('',*,*,#1980,.F.);
#2520=ORIENTED_EDGE('',*,*,#1973,.T.);
#2521=ORIENTED_EDGE('',*,*,#1981,.F.);
#2522=ORIENTED_EDGE('',*,*,#1977,.T.);
#2523=ORIENTED_EDGE('',*,*,#1982,.F.);
#2524=ORIENTED_EDGE('',*,*,#1983,.T.);
#2525=ORIENTED_EDGE('',*,*,#1984,.T.);
#2526=ORIENTED_EDGE('',*,*,#1985,.F.);
#2527=ORIENTED_EDGE('',*,*,#1986,.T.);
#2528=ORIENTED_EDGE('',*,*,#1983,.F.);
#2529=ORIENTED_EDGE('',*,*,#1986,.F.);
#2530=ORIENTED_EDGE('',*,*,#1985,.T.);
#2531=ORIENTED_EDGE('',*,*,#1987,.F.);
#2532=ORIENTED_EDGE('',*,*,#1988,.T.);
#2533=ORIENTED_EDGE('',*,*,#1984,.F.);
#2534=ORIENTED_EDGE('',*,*,#1988,.F.);
#2535=ORIENTED_EDGE('',*,*,#1987,.T.);
#2536=ORIENTED_EDGE('',*,*,#1974,.T.);
#2537=ORIENTED_EDGE('',*,*,#1982,.T.);
#2538=ORIENTED_EDGE('',*,*,#1980,.T.);
#2539=ORIENTED_EDGE('',*,*,#1989,.F.);
#2540=ORIENTED_EDGE('',*,*,#1976,.T.);
#2541=ORIENTED_EDGE('',*,*,#1990,.F.);
#2542=ORIENTED_EDGE('',*,*,#1978,.T.);
#2543=ORIENTED_EDGE('',*,*,#1981,.T.);
#2544=ORIENTED_EDGE('',*,*,#1975,.T.);
#2545=ORIENTED_EDGE('',*,*,#1989,.T.);
#2546=ORIENTED_EDGE('',*,*,#1979,.T.);
#2547=ORIENTED_EDGE('',*,*,#1990,.T.);
#3483=CYLINDRICAL_SURFACE('',#3949,1.1);
#3484=CYLINDRICAL_SURFACE('',#3952,1.1);
#3485=CYLINDRICAL_SURFACE('',#3955,4.99999999999999);
#3486=CYLINDRICAL_SURFACE('',#3957,33.8);
#3553=ADVANCED_FACE('',(#347),#194,.F.);
#3554=ADVANCED_FACE('',(#348),#195,.F.);
#3555=ADVANCED_FACE('',(#349,#132,#133),#196,.F.);
#3556=ADVANCED_FACE('',(#350),#3483,.T.);
#3557=ADVANCED_FACE('',(#351),#197,.F.);
#3558=ADVANCED_FACE('',(#352),#3484,.T.);
#3559=ADVANCED_FACE('',(#353),#198,.F.);
#3560=ADVANCED_FACE('',(#354),#3485,.F.);
#3561=ADVANCED_FACE('',(#355),#3486,.T.);
#3562=ADVANCED_FACE('',(#356),#199,.T.);
#3754=CLOSED_SHELL('',(#3553,#3554,#3555,#3556,#3557,#3558,#3559,#3560,
#3561,#3562));
#3941=AXIS2_PLACEMENT_3D('',#5627,#4442,#4443);
#3942=AXIS2_PLACEMENT_3D('',#5628,#4444,#4445);
#3943=AXIS2_PLACEMENT_3D('',#5637,#4450,#4451);
#3944=AXIS2_PLACEMENT_3D('',#5646,#4456,#4457);
#3945=AXIS2_PLACEMENT_3D('',#5647,#4458,#4459);
#3946=AXIS2_PLACEMENT_3D('',#5648,#4460,#4461);
#3947=AXIS2_PLACEMENT_3D('',#5650,#4462,#4463);
#3948=AXIS2_PLACEMENT_3D('',#5652,#4464,#4465);
#3949=AXIS2_PLACEMENT_3D('',#5653,#4466,#4467);
#3950=AXIS2_PLACEMENT_3D('',#5655,#4468,#4469);
#3951=AXIS2_PLACEMENT_3D('',#5657,#4471,#4472);
#3952=AXIS2_PLACEMENT_3D('',#5658,#4473,#4474);
#3953=AXIS2_PLACEMENT_3D('',#5660,#4475,#4476);
#3954=AXIS2_PLACEMENT_3D('',#5662,#4478,#4479);
#3955=AXIS2_PLACEMENT_3D('',#5663,#4480,#4481);
#3956=AXIS2_PLACEMENT_3D('',#5664,#4482,#4483);
#3957=AXIS2_PLACEMENT_3D('',#5665,#4484,#4485);
#3958=AXIS2_PLACEMENT_3D('',#5666,#4486,#4487);
#3959=AXIS2_PLACEMENT_3D('',#5667,#4488,#4489);
#4442=DIRECTION('axis',(0.,0.,1.));
#4443=DIRECTION('refdir',(1.,0.,0.));
#4444=DIRECTION('center_axis',(-0.707106781186547,0.,0.707106781186548));
#4445=DIRECTION('ref_axis',(0.707106781186548,0.,0.707106781186547));
#4446=DIRECTION('',(0.707106781186548,0.,0.707106781186547));
#4447=DIRECTION('',(0.,-1.,0.));
#4448=DIRECTION('',(-0.707106781186548,0.,-0.707106781186547));
#4449=DIRECTION('',(0.,1.,0.));
#4450=DIRECTION('center_axis',(1.,0.,0.));
#4451=DIRECTION('ref_axis',(0.,0.,-1.));
#4452=DIRECTION('',(0.,0.,-1.));
#4453=DIRECTION('',(0.,-1.,0.));
#4454=DIRECTION('',(0.,0.,1.));
#4455=DIRECTION('',(0.,1.,0.));
#4456=DIRECTION('center_axis',(0.,1.,0.));
#4457=DIRECTION('ref_axis',(1.,0.,0.));
#4458=DIRECTION('center_axis',(0.,1.,0.));
#4459=DIRECTION('ref_axis',(1.,0.,0.));
#4460=DIRECTION('center_axis',(0.,-1.,0.));
#4461=DIRECTION('ref_axis',(1.,0.,0.));
#4462=DIRECTION('center_axis',(0.,1.,0.));
#4463=DIRECTION('ref_axis',(1.,0.,0.));
#4464=DIRECTION('center_axis',(0.,1.,0.));
#4465=DIRECTION('ref_axis',(1.,0.,0.));
#4466=DIRECTION('center_axis',(0.,-1.,0.));
#4467=DIRECTION('ref_axis',(1.,0.,0.));
#4468=DIRECTION('center_axis',(0.,-1.,0.));
#4469=DIRECTION('ref_axis',(1.,0.,0.));
#4470=DIRECTION('',(0.,1.,0.));
#4471=DIRECTION('center_axis',(0.,1.,0.));
#4472=DIRECTION('ref_axis',(1.,0.,0.));
#4473=DIRECTION('center_axis',(0.,-1.,0.));
#4474=DIRECTION('ref_axis',(1.,0.,0.));
#4475=DIRECTION('center_axis',(0.,-1.,0.));
#4476=DIRECTION('ref_axis',(1.,0.,0.));
#4477=DIRECTION('',(0.,1.,0.));
#4478=DIRECTION('center_axis',(0.,1.,0.));
#4479=DIRECTION('ref_axis',(1.,0.,0.));
#4480=DIRECTION('center_axis',(0.,1.,0.));
#4481=DIRECTION('ref_axis',(1.,0.,0.));
#4482=DIRECTION('center_axis',(0.,-1.,0.));
#4483=DIRECTION('ref_axis',(1.,0.,0.));
#4484=DIRECTION('center_axis',(0.,1.,0.));
#4485=DIRECTION('ref_axis',(1.,0.,0.));
#4486=DIRECTION('center_axis',(0.,1.,0.));
#4487=DIRECTION('ref_axis',(1.,0.,0.));
#4488=DIRECTION('center_axis',(0.,1.,0.));
#4489=DIRECTION('ref_axis',(1.,0.,0.));
#5627=CARTESIAN_POINT('',(0.,0.,0.));
#5628=CARTESIAN_POINT('Origin',(3.53553390593273,-3.,117.867942062963));
#5629=CARTESIAN_POINT('',(3.53553390593273,-3.,117.867942062963));
#5630=CARTESIAN_POINT('',(23.9002092041053,-3.,138.232617361136));
#5631=CARTESIAN_POINT('',(1.76776695296637,-3.,116.100175109997));
#5632=CARTESIAN_POINT('',(3.53553390593273,-2.9,117.867942062963));
#5633=CARTESIAN_POINT('',(3.53553390593273,-3.,117.867942062963));
#5634=CARTESIAN_POINT('',(23.9002092041053,-2.9,138.232617361136));
#5635=CARTESIAN_POINT('',(1.76776695296637,-2.9,116.100175109997));
#5636=CARTESIAN_POINT('',(23.9002092041053,-3.,138.232617361136));
#5637=CARTESIAN_POINT('Origin',(-2.22044604925031E-15,-3.,148.13240815703));
#5638=CARTESIAN_POINT('',(-2.22044604925031E-15,-3.,148.13240815703));
#5639=CARTESIAN_POINT('',(-2.22044604925031E-15,-3.,119.33240815703));
#5640=CARTESIAN_POINT('',(-2.22044604925031E-15,-3.,131.23240815703));
#5641=CARTESIAN_POINT('',(-2.22044604925031E-15,-2.9,148.13240815703));
#5642=CARTESIAN_POINT('',(-2.22044604925031E-15,-3.,148.13240815703));
#5643=CARTESIAN_POINT('',(-2.22044604925031E-15,-2.9,119.33240815703));
#5644=CARTESIAN_POINT('',(-2.22044604925031E-15,-2.9,131.23240815703));
#5645=CARTESIAN_POINT('',(-2.22044604925031E-15,-3.,119.33240815703));
#5646=CARTESIAN_POINT('Origin',(0.,-3.,114.33240815703));
#5647=CARTESIAN_POINT('Origin',(-2.22044604925031E-15,-3.,114.33240815703));
#5648=CARTESIAN_POINT('Origin',(-2.22044604925031E-15,-3.,114.33240815703));
#5649=CARTESIAN_POINT('',(5.20441727387071,-3.,142.877430577928));
#5650=CARTESIAN_POINT('Origin',(6.30441727387071,-3.,142.877430577928));
#5651=CARTESIAN_POINT('',(15.6482292407074,-3.,138.291974085347));
#5652=CARTESIAN_POINT('Origin',(16.7482292407074,-3.,138.291974085347));
#5653=CARTESIAN_POINT('Origin',(6.30441727387071,-3.,142.877430577928));
#5654=CARTESIAN_POINT('',(5.20441727387071,-3.5,142.877430577928));
#5655=CARTESIAN_POINT('Origin',(6.30441727387071,-3.5,142.877430577928));
#5656=CARTESIAN_POINT('',(5.20441727387071,-3.,142.877430577928));
#5657=CARTESIAN_POINT('Origin',(6.30441727387071,-3.5,142.877430577928));
#5658=CARTESIAN_POINT('Origin',(16.7482292407074,-3.,138.291974085347));
#5659=CARTESIAN_POINT('',(15.6482292407074,-3.5,138.291974085347));
#5660=CARTESIAN_POINT('Origin',(16.7482292407074,-3.5,138.291974085347));
#5661=CARTESIAN_POINT('',(15.6482292407074,-3.,138.291974085347));
#5662=CARTESIAN_POINT('Origin',(16.7482292407074,-3.5,138.291974085347));
#5663=CARTESIAN_POINT('Origin',(-2.22044604925031E-15,-3.,114.33240815703));
#5664=CARTESIAN_POINT('Origin',(-2.22044604925031E-15,-2.9,114.33240815703));
#5665=CARTESIAN_POINT('Origin',(-2.22044604925031E-15,-3.,114.33240815703));
#5666=CARTESIAN_POINT('Origin',(-2.22044604925031E-15,-2.9,114.33240815703));
#5667=CARTESIAN_POINT('Origin',(0.,-2.9,114.33240815703));
#6727=UNCERTAINTY_MEASURE_WITH_UNIT(LENGTH_MEASURE(0.01),#6754,
'DISTANCE_ACCURACY_VALUE',
'Maximum model space distance between geometric entities at asserted c
onnectivities');
#6738=UNCERTAINTY_MEASURE_WITH_UNIT(LENGTH_MEASURE(0.01),#6754,
'DISTANCE_ACCURACY_VALUE',
'Maximum model space distance between geometric entities at asserted c
onnectivities');
#6742=(
GEOMETRIC_REPRESENTATION_CONTEXT(3)
GLOBAL_UNCERTAINTY_ASSIGNED_CONTEXT((#6727))
GLOBAL_UNIT_ASSIGNED_CONTEXT((#6754,#6756,#6757))
REPRESENTATION_CONTEXT('','3D')
);
#6753=(
GEOMETRIC_REPRESENTATION_CONTEXT(3)
GLOBAL_UNCERTAINTY_ASSIGNED_CONTEXT((#6738))
GLOBAL_UNIT_ASSIGNED_CONTEXT((#6754,#6756,#6757))
REPRESENTATION_CONTEXT('','3D')
);
#6754=(
LENGTH_UNIT()
NAMED_UNIT(*)
SI_UNIT(.MILLI.,.METRE.)
);
#6756=(
NAMED_UNIT(*)
PLANE_ANGLE_UNIT()
SI_UNIT($,.RADIAN.)
);
#6757=(
NAMED_UNIT(*)
SI_UNIT($,.STERADIAN.)
SOLID_ANGLE_UNIT()
);
#6761=SHAPE_DEFINITION_REPRESENTATION(#6775,#6802);
#6775=PRODUCT_DEFINITION_SHAPE('',$,#6817);
#6802=SHAPE_REPRESENTATION('',(#3941),#6742);
#6813=PRODUCT_DEFINITION_CONTEXT('part definition',#6857,'design');
#6817=PRODUCT_DEFINITION('Blade_01','Blade_01',#6831,#6813);
#6831=PRODUCT_DEFINITION_FORMATION('',$,#6862);
#6857=APPLICATION_CONTEXT(
'Core Data for Automotive Mechanical Design Process');
#6858=PRODUCT_CONTEXT('part definition',#6857,'mechanical');
#6862=PRODUCT('Blade_01','Blade_01',$,(#6858));
#6929=COLOUR_RGB('Off White',0.89,0.88,0.83);
#6930=FILL_AREA_STYLE_COLOUR('',#6929);
#6931=FILL_AREA_STYLE('',(#6930));
#6932=SURFACE_STYLE_FILL_AREA(#6931);
#6933=SURFACE_SIDE_STYLE('',(#6932));
#6934=SURFACE_STYLE_USAGE(.BOTH.,#6933);
#6935=PRESENTATION_STYLE_ASSIGNMENT((#6934));
ENDSEC;
END-ISO-10303-21;
